ISO-10303-21;
HEADER;
/* Generated by software containing ST-Developer
 * from STEP Tools, Inc. (www.steptools.com) 
 */

FILE_DESCRIPTION(
/* description */ ('Timing belt drive module 2 mm Pitch Timing 20T-40T'),

/* implementation_level */ '2;1');

FILE_NAME(
/* name */ 'M4x10 Cap Screw.step',
/* time_stamp */ '2026-10-28T03:25:12-07:00',
/* author */ (''),
/* organization */ (''),
/* preprocessor_version */ 'ST-DEVELOPER v20.2',
/* originating_system */ 'Autodesk Translation Framework v15.17.0.0',
/* authorisation */ '');

FILE_SCHEMA (('AUTOMOTIVE_DESIGN { 1 0 10303 214 3 1 1 }'));
ENDSEC;

DATA;
#10=MECHANICAL_DESIGN_GEOMETRIC_PRESENTATION_REPRESENTATION('',(#566),#17830);
#12=ORIENTED_CLOSED_SHELL('',*,#9024,.F.);
#15=BREP_WITH_VOIDS('Body1',#9025,(#12));
#427=CONICAL_SURFACE('',#10181,0.325,0.785398163397448);
#428=CONICAL_SURFACE('',#10185,0.335,0.785398163397448);
#429=CONICAL_SURFACE('',#10189,0.21,0.463647609000806);
#465=SHAPE_REPRESENTATION_RELATIONSHIP('SRR','None',#18037,#508);
#508=ADVANCED_BREP_SHAPE_REPRESENTATION('',(#15),#17812);
#566=STYLED_ITEM('',(#18324),#15);
#729=FACE_BOUND('',#1873,.T.);
#898=PLANE('',#10169);
#899=PLANE('',#10170);
#900=PLANE('',#10171);
#901=PLANE('',#10172);
#902=PLANE('',#10173);
#903=PLANE('',#10174);
#904=PLANE('',#10175);
#905=PLANE('',#10176);
#906=PLANE('',#10177);
#907=PLANE('',#10179);
#908=PLANE('',#10187);
#1246=FACE_OUTER_BOUND('',#1859,.T.);
#1247=FACE_OUTER_BOUND('',#1860,.T.);
#1248=FACE_OUTER_BOUND('',#1861,.T.);
#1249=FACE_OUTER_BOUND('',#1862,.T.);
#1250=FACE_OUTER_BOUND('',#1863,.T.);
#1251=FACE_OUTER_BOUND('',#1864,.T.);
#1252=FACE_OUTER_BOUND('',#1865,.T.);
#1253=FACE_OUTER_BOUND('',#1866,.T.);
#1254=FACE_OUTER_BOUND('',#1867,.T.);
#1255=FACE_OUTER_BOUND('',#1868,.T.);
#1256=FACE_OUTER_BOUND('',#1869,.T.);
#1257=FACE_OUTER_BOUND('',#1870,.T.);
#1258=FACE_OUTER_BOUND('',#1871,.T.);
#1259=FACE_OUTER_BOUND('',#1872,.T.);
#1260=FACE_OUTER_BOUND('',#1874,.T.);
#1261=FACE_OUTER_BOUND('',#1875,.T.);
#1859=EDGE_LOOP('',(#7021,#7022,#7023,#7024));
#1860=EDGE_LOOP('',(#7025,#7026,#7027,#7028));
#1861=EDGE_LOOP('',(#7029,#7030,#7031,#7032));
#1862=EDGE_LOOP('',(#7033,#7034,#7035,#7036));
#1863=EDGE_LOOP('',(#7037,#7038,#7039,#7040));
#1864=EDGE_LOOP('',(#7041,#7042,#7043,#7044));
#1865=EDGE_LOOP('',(#7045,#7046,#7047,#7048,#7049,#7050));
#1866=EDGE_LOOP('',(#7051,#7052,#7053,#7054,#7055,#7056));
#1867=EDGE_LOOP('',(#7057));
#1868=EDGE_LOOP('',(#7058));
#1869=EDGE_LOOP('',(#7059,#7060,#7061,#7062));
#1870=EDGE_LOOP('',(#7063,#7064,#7065,#7066));
#1871=EDGE_LOOP('',(#7067,#7068,#7069,#7070));
#1872=EDGE_LOOP('',(#7071));
#1873=EDGE_LOOP('',(#7072));
#1874=EDGE_LOOP('',(#7073,#7074,#7075,#7076));
#1875=EDGE_LOOP('',(#7077,#7078,#7079,#7080));
#2467=CIRCLE('',#10178,0.1954);
#2468=CIRCLE('',#10180,0.3);
#2469=CIRCLE('',#10182,0.35);
#2470=CIRCLE('',#10184,0.35);
#2471=CIRCLE('',#10186,0.32);
#2472=CIRCLE('',#10188,0.22);
#2473=CIRCLE('',#10190,0.1954);
#3055=LINE('',#15890,#3533);
#3056=LINE('',#15892,#3534);
#3057=LINE('',#15894,#3535);
#3058=LINE('',#15895,#3536);
#3059=LINE('',#15898,#3537);
#3060=LINE('',#15900,#3538);
#3061=LINE('',#15901,#3539);
#3062=LINE('',#15904,#3540);
#3063=LINE('',#15906,#3541);
#3064=LINE('',#15907,#3542);
#3065=LINE('',#15910,#3543);
#3066=LINE('',#15912,#3544);
#3067=LINE('',#15913,#3545);
#3068=LINE('',#15916,#3546);
#3069=LINE('',#15918,#3547);
#3070=LINE('',#15919,#3548);
#3071=LINE('',#15921,#3549);
#3072=LINE('',#15922,#3550);
#3073=LINE('',#15934,#3551);
#3074=LINE('',#15938,#3552);
#3075=LINE('',#15942,#3553);
#3076=LINE('',#15949,#3554);
#3077=LINE('',#15951,#3555);
#3533=VECTOR('',#12382,1.);
#3534=VECTOR('',#12383,1.);
#3535=VECTOR('',#12384,1.);
#3536=VECTOR('',#12385,1.);
#3537=VECTOR('',#12388,1.);
#3538=VECTOR('',#12389,1.);
#3539=VECTOR('',#12390,1.);
#3540=VECTOR('',#12393,1.);
#3541=VECTOR('',#12394,1.);
#3542=VECTOR('',#12395,1.);
#3543=VECTOR('',#12398,1.);
#3544=VECTOR('',#12399,1.);
#3545=VECTOR('',#12400,1.);
#3546=VECTOR('',#12403,1.);
#3547=VECTOR('',#12404,1.);
#3548=VECTOR('',#12405,1.);
#3549=VECTOR('',#12408,1.);
#3550=VECTOR('',#12409,1.);
#3551=VECTOR('',#12426,0.325);
#3552=VECTOR('',#12431,0.35);
#3553=VECTOR('',#12436,0.335);
#3554=VECTOR('',#12445,0.21);
#3555=VECTOR('',#12448,0.2);
#4178=VERTEX_POINT('',#15888);
#4179=VERTEX_POINT('',#15889);
#4180=VERTEX_POINT('',#15891);
#4181=VERTEX_POINT('',#15893);
#4182=VERTEX_POINT('',#15897);
#4183=VERTEX_POINT('',#15899);
#4184=VERTEX_POINT('',#15903);
#4185=VERTEX_POINT('',#15905);
#4186=VERTEX_POINT('',#15909);
#4187=VERTEX_POINT('',#15911);
#4188=VERTEX_POINT('',#15915);
#4189=VERTEX_POINT('',#15917);
#4190=VERTEX_POINT('',#15926);
#4191=VERTEX_POINT('',#15929);
#4192=VERTEX_POINT('',#15932);
#4193=VERTEX_POINT('',#15936);
#4194=VERTEX_POINT('',#15940);
#4195=VERTEX_POINT('',#15944);
#4196=VERTEX_POINT('',#15947);
#5193=EDGE_CURVE('',#4178,#4179,#3055,.T.);
#5194=EDGE_CURVE('',#4179,#4180,#3056,.T.);
#5195=EDGE_CURVE('',#4180,#4181,#3057,.T.);
#5196=EDGE_CURVE('',#4178,#4181,#3058,.T.);
#5197=EDGE_CURVE('',#4179,#4182,#3059,.T.);
#5198=EDGE_CURVE('',#4182,#4183,#3060,.T.);
#5199=EDGE_CURVE('',#4183,#4180,#3061,.T.);
#5200=EDGE_CURVE('',#4182,#4184,#3062,.T.);
#5201=EDGE_CURVE('',#4184,#4185,#3063,.T.);
#5202=EDGE_CURVE('',#4185,#4183,#3064,.T.);
#5203=EDGE_CURVE('',#4184,#4186,#3065,.T.);
#5204=EDGE_CURVE('',#4186,#4187,#3066,.T.);
#5205=EDGE_CURVE('',#4187,#4185,#3067,.T.);
#5206=EDGE_CURVE('',#4186,#4188,#3068,.T.);
#5207=EDGE_CURVE('',#4188,#4189,#3069,.T.);
#5208=EDGE_CURVE('',#4189,#4187,#3070,.T.);
#5209=EDGE_CURVE('',#4188,#4178,#3071,.T.);
#5210=EDGE_CURVE('',#4181,#4189,#3072,.T.);
#5211=EDGE_CURVE('',#4190,#4190,#2467,.T.);
#5212=EDGE_CURVE('',#4191,#4191,#2468,.T.);
#5213=EDGE_CURVE('',#4192,#4192,#2469,.T.);
#5214=EDGE_CURVE('',#4192,#4191,#3073,.T.);
#5215=EDGE_CURVE('',#4193,#4193,#2470,.T.);
#5216=EDGE_CURVE('',#4193,#4192,#3074,.T.);
#5217=EDGE_CURVE('',#4194,#4194,#2471,.T.);
#5218=EDGE_CURVE('',#4194,#4193,#3075,.T.);
#5219=EDGE_CURVE('',#4195,#4195,#2472,.T.);
#5220=EDGE_CURVE('',#4196,#4196,#2473,.F.);
#5221=EDGE_CURVE('',#4196,#4195,#3076,.T.);
#5222=EDGE_CURVE('',#4190,#4196,#3077,.T.);
#7021=ORIENTED_EDGE('',*,*,#5193,.T.);
#7022=ORIENTED_EDGE('',*,*,#5194,.T.);
#7023=ORIENTED_EDGE('',*,*,#5195,.T.);
#7024=ORIENTED_EDGE('',*,*,#5196,.F.);
#7025=ORIENTED_EDGE('',*,*,#5197,.T.);
#7026=ORIENTED_EDGE('',*,*,#5198,.T.);
#7027=ORIENTED_EDGE('',*,*,#5199,.T.);
#7028=ORIENTED_EDGE('',*,*,#5194,.F.);
#7029=ORIENTED_EDGE('',*,*,#5200,.T.);
#7030=ORIENTED_EDGE('',*,*,#5201,.T.);
#7031=ORIENTED_EDGE('',*,*,#5202,.T.);
#7032=ORIENTED_EDGE('',*,*,#5198,.F.);
#7033=ORIENTED_EDGE('',*,*,#5203,.T.);
#7034=ORIENTED_EDGE('',*,*,#5204,.T.);
#7035=ORIENTED_EDGE('',*,*,#5205,.T.);
#7036=ORIENTED_EDGE('',*,*,#5201,.F.);
#7037=ORIENTED_EDGE('',*,*,#5206,.T.);
#7038=ORIENTED_EDGE('',*,*,#5207,.T.);
#7039=ORIENTED_EDGE('',*,*,#5208,.T.);
#7040=ORIENTED_EDGE('',*,*,#5204,.F.);
#7041=ORIENTED_EDGE('',*,*,#5209,.T.);
#7042=ORIENTED_EDGE('',*,*,#5196,.T.);
#7043=ORIENTED_EDGE('',*,*,#5210,.T.);
#7044=ORIENTED_EDGE('',*,*,#5207,.F.);
#7045=ORIENTED_EDGE('',*,*,#5209,.F.);
#7046=ORIENTED_EDGE('',*,*,#5206,.F.);
#7047=ORIENTED_EDGE('',*,*,#5203,.F.);
#7048=ORIENTED_EDGE('',*,*,#5200,.F.);
#7049=ORIENTED_EDGE('',*,*,#5197,.F.);
#7050=ORIENTED_EDGE('',*,*,#5193,.F.);
#7051=ORIENTED_EDGE('',*,*,#5210,.F.);
#7052=ORIENTED_EDGE('',*,*,#5195,.F.);
#7053=ORIENTED_EDGE('',*,*,#5199,.F.);
#7054=ORIENTED_EDGE('',*,*,#5202,.F.);
#7055=ORIENTED_EDGE('',*,*,#5205,.F.);
#7056=ORIENTED_EDGE('',*,*,#5208,.F.);
#7057=ORIENTED_EDGE('',*,*,#5211,.F.);
#7058=ORIENTED_EDGE('',*,*,#5212,.F.);
#7059=ORIENTED_EDGE('',*,*,#5213,.F.);
#7060=ORIENTED_EDGE('',*,*,#5214,.T.);
#7061=ORIENTED_EDGE('',*,*,#5212,.T.);
#7062=ORIENTED_EDGE('',*,*,#5214,.F.);
#7063=ORIENTED_EDGE('',*,*,#5215,.F.);
#7064=ORIENTED_EDGE('',*,*,#5216,.T.);
#7065=ORIENTED_EDGE('',*,*,#5213,.T.);
#7066=ORIENTED_EDGE('',*,*,#5216,.F.);
#7067=ORIENTED_EDGE('',*,*,#5217,.F.);
#7068=ORIENTED_EDGE('',*,*,#5218,.T.);
#7069=ORIENTED_EDGE('',*,*,#5215,.T.);
#7070=ORIENTED_EDGE('',*,*,#5218,.F.);
#7071=ORIENTED_EDGE('',*,*,#5217,.T.);
#7072=ORIENTED_EDGE('',*,*,#5219,.F.);
#7073=ORIENTED_EDGE('',*,*,#5220,.F.);
#7074=ORIENTED_EDGE('',*,*,#5221,.T.);
#7075=ORIENTED_EDGE('',*,*,#5219,.T.);
#7076=ORIENTED_EDGE('',*,*,#5221,.F.);
#7077=ORIENTED_EDGE('',*,*,#5211,.T.);
#7078=ORIENTED_EDGE('',*,*,#5222,.T.);
#7079=ORIENTED_EDGE('',*,*,#5220,.T.);
#7080=ORIENTED_EDGE('',*,*,#5222,.F.);
#8294=CYLINDRICAL_SURFACE('',#10183,0.35);
#8295=CYLINDRICAL_SURFACE('',#10191,0.1954);
#8744=ADVANCED_FACE('',(#1246),#898,.F.);
#8745=ADVANCED_FACE('',(#1247),#899,.F.);
#8746=ADVANCED_FACE('',(#1248),#900,.F.);
#8747=ADVANCED_FACE('',(#1249),#901,.F.);
#8748=ADVANCED_FACE('',(#1250),#902,.F.);
#8749=ADVANCED_FACE('',(#1251),#903,.F.);
#8750=ADVANCED_FACE('',(#1252),#904,.F.);
#8751=ADVANCED_FACE('',(#1253),#905,.F.);
#8752=ADVANCED_FACE('',(#1254),#906,.F.);
#8753=ADVANCED_FACE('',(#1255),#907,.T.);
#8754=ADVANCED_FACE('',(#1256),#427,.T.);
#8755=ADVANCED_FACE('',(#1257),#8294,.T.);
#8756=ADVANCED_FACE('',(#1258),#428,.T.);
#8757=ADVANCED_FACE('',(#1259,#729),#908,.T.);
#8758=ADVANCED_FACE('',(#1260),#429,.T.);
#8759=ADVANCED_FACE('',(#1261),#8295,.T.);
#9024=CLOSED_SHELL('',(#8744,#8745,#8746,#8747,#8748,#8749,#8750,#8751));
#9025=CLOSED_SHELL('',(#8752,#8753,#8754,#8755,#8756,#8757,#8758,#8759));
#10168=AXIS2_PLACEMENT_3D('',#15886,#12378,#12379);
#10169=AXIS2_PLACEMENT_3D('',#15887,#12380,#12381);
#10170=AXIS2_PLACEMENT_3D('',#15896,#12386,#12387);
#10171=AXIS2_PLACEMENT_3D('',#15902,#12391,#12392);
#10172=AXIS2_PLACEMENT_3D('',#15908,#12396,#12397);
#10173=AXIS2_PLACEMENT_3D('',#15914,#12401,#12402);
#10174=AXIS2_PLACEMENT_3D('',#15920,#12406,#12407);
#10175=AXIS2_PLACEMENT_3D('',#15923,#12410,#12411);
#10176=AXIS2_PLACEMENT_3D('',#15924,#12412,#12413);
#10177=AXIS2_PLACEMENT_3D('',#15925,#12414,#12415);
#10178=AXIS2_PLACEMENT_3D('',#15927,#12416,#12417);
#10179=AXIS2_PLACEMENT_3D('',#15928,#12418,#12419);
#10180=AXIS2_PLACEMENT_3D('',#15930,#12420,#12421);
#10181=AXIS2_PLACEMENT_3D('',#15931,#12422,#12423);
#10182=AXIS2_PLACEMENT_3D('',#15933,#12424,#12425);
#10183=AXIS2_PLACEMENT_3D('',#15935,#12427,#12428);
#10184=AXIS2_PLACEMENT_3D('',#15937,#12429,#12430);
#10185=AXIS2_PLACEMENT_3D('',#15939,#12432,#12433);
#10186=AXIS2_PLACEMENT_3D('',#15941,#12434,#12435);
#10187=AXIS2_PLACEMENT_3D('',#15943,#12437,#12438);
#10188=AXIS2_PLACEMENT_3D('',#15945,#12439,#12440);
#10189=AXIS2_PLACEMENT_3D('',#15946,#12441,#12442);
#10190=AXIS2_PLACEMENT_3D('',#15948,#12443,#12444);
#10191=AXIS2_PLACEMENT_3D('',#15950,#12446,#12447);
#12378=DIRECTION('axis',(0.,0.,1.));
#12379=DIRECTION('refdir',(1.,0.,0.));
#12380=DIRECTION('center_axis',(0.866025403784439,0.,-0.5));
#12381=DIRECTION('ref_axis',(0.5,0.,0.866025403784439));
#12382=DIRECTION('',(-0.5,0.,-0.866025403784439));
#12383=DIRECTION('',(0.,-1.,0.));
#12384=DIRECTION('',(0.5,0.,0.866025403784439));
#12385=DIRECTION('',(0.,-1.,0.));
#12386=DIRECTION('center_axis',(1.60246890531964E-16,0.,-1.));
#12387=DIRECTION('ref_axis',(1.,0.,1.60246890531964E-16));
#12388=DIRECTION('',(-1.,0.,-1.60246890531964E-16));
#12389=DIRECTION('',(0.,-1.,0.));
#12390=DIRECTION('',(1.,0.,1.60246890531964E-16));
#12391=DIRECTION('center_axis',(-0.866025403784439,0.,-0.5));
#12392=DIRECTION('ref_axis',(0.5,0.,-0.866025403784439));
#12393=DIRECTION('',(-0.5,0.,0.866025403784439));
#12394=DIRECTION('',(0.,-1.,0.));
#12395=DIRECTION('',(0.5,0.,-0.866025403784439));
#12396=DIRECTION('center_axis',(-0.866025403784439,0.,0.5));
#12397=DIRECTION('ref_axis',(-0.5,0.,-0.866025403784439));
#12398=DIRECTION('',(0.5,0.,0.866025403784439));
#12399=DIRECTION('',(0.,-1.,0.));
#12400=DIRECTION('',(-0.5,0.,-0.866025403784439));
#12401=DIRECTION('center_axis',(-1.60246890531964E-16,0.,1.));
#12402=DIRECTION('ref_axis',(-1.,0.,-1.60246890531964E-16));
#12403=DIRECTION('',(1.,0.,1.60246890531964E-16));
#12404=DIRECTION('',(0.,-1.,0.));
#12405=DIRECTION('',(-1.,0.,-1.60246890531964E-16));
#12406=DIRECTION('center_axis',(0.866025403784439,0.,0.5));
#12407=DIRECTION('ref_axis',(-0.5,0.,0.866025403784439));
#12408=DIRECTION('',(0.5,0.,-0.866025403784439));
#12409=DIRECTION('',(-0.5,0.,0.866025403784439));
#12410=DIRECTION('center_axis',(0.,1.,0.));
#12411=DIRECTION('ref_axis',(1.,0.,0.));
#12412=DIRECTION('center_axis',(0.,-1.,0.));
#12413=DIRECTION('ref_axis',(0.,0.,-1.));
#12414=DIRECTION('center_axis',(0.,1.,0.));
#12415=DIRECTION('ref_axis',(1.,0.,0.));
#12416=DIRECTION('center_axis',(0.,1.,0.));
#12417=DIRECTION('ref_axis',(1.,0.,0.));
#12418=DIRECTION('center_axis',(0.,1.,0.));
#12419=DIRECTION('ref_axis',(0.,0.,1.));
#12420=DIRECTION('center_axis',(0.,-1.,0.));
#12421=DIRECTION('ref_axis',(1.,0.,0.));
#12422=DIRECTION('center_axis',(0.,-1.,0.));
#12423=DIRECTION('ref_axis',(1.,0.,0.));
#12424=DIRECTION('center_axis',(0.,-1.,0.));
#12425=DIRECTION('ref_axis',(1.,0.,0.));
#12426=DIRECTION('',(0.707106781186547,0.707106781186548,8.65956056235493E-17));
#12427=DIRECTION('center_axis',(0.,-1.,0.));
#12428=DIRECTION('ref_axis',(1.,0.,0.));
#12429=DIRECTION('center_axis',(0.,-1.,0.));
#12430=DIRECTION('ref_axis',(1.,0.,0.));
#12431=DIRECTION('',(0.,1.,0.));
#12432=DIRECTION('center_axis',(0.,1.,0.));
#12433=DIRECTION('ref_axis',(1.,0.,0.));
#12434=DIRECTION('center_axis',(0.,-1.,0.));
#12435=DIRECTION('ref_axis',(1.,0.,0.));
#12436=DIRECTION('',(-0.707106781186547,0.707106781186548,-8.65956056235493E-17));
#12437=DIRECTION('center_axis',(0.,-1.,0.));
#12438=DIRECTION('ref_axis',(0.,0.,-1.));
#12439=DIRECTION('center_axis',(0.,-1.,0.));
#12440=DIRECTION('ref_axis',(1.,0.,0.));
#12441=DIRECTION('center_axis',(0.,1.,0.));
#12442=DIRECTION('ref_axis',(1.,0.,0.));
#12443=DIRECTION('center_axis',(0.,1.,0.));
#12444=DIRECTION('ref_axis',(1.,0.,0.));
#12445=DIRECTION('',(-0.447213595499958,0.894427190999916,-5.47678698264203E-17));
#12446=DIRECTION('center_axis',(0.,-1.,0.));
#12447=DIRECTION('ref_axis',(1.,0.,0.));
#12448=DIRECTION('',(0.,1.,0.));
#15886=CARTESIAN_POINT('',(0.,0.,0.));
#15887=CARTESIAN_POINT('Origin',(0.0866025403784439,-0.4,-0.15));
#15888=CARTESIAN_POINT('',(0.173205080756888,-0.4,0.));
#15889=CARTESIAN_POINT('',(0.0866025403784439,-0.4,-0.15));
#15890=CARTESIAN_POINT('',(0.173205080756888,-0.4,0.));
#15891=CARTESIAN_POINT('',(0.0866025403784439,-0.64,-0.15));
#15892=CARTESIAN_POINT('',(0.0866025403784439,-0.4,-0.15));
#15893=CARTESIAN_POINT('',(0.173205080756888,-0.64,0.));
#15894=CARTESIAN_POINT('',(0.173205080756888,-0.64,0.));
#15895=CARTESIAN_POINT('',(0.173205080756888,-0.4,0.));
#15896=CARTESIAN_POINT('Origin',(-0.0866025403784438,-0.4,-0.15));
#15897=CARTESIAN_POINT('',(-0.0866025403784438,-0.4,-0.15));
#15898=CARTESIAN_POINT('',(0.0866025403784439,-0.4,-0.15));
#15899=CARTESIAN_POINT('',(-0.0866025403784438,-0.64,-0.15));
#15900=CARTESIAN_POINT('',(-0.0866025403784438,-0.4,-0.15));
#15901=CARTESIAN_POINT('',(0.0866025403784439,-0.64,-0.15));
#15902=CARTESIAN_POINT('Origin',(-0.173205080756888,-0.4,-2.77555756156289E-17));
#15903=CARTESIAN_POINT('',(-0.173205080756888,-0.4,-2.12115047744981E-17));
#15904=CARTESIAN_POINT('',(-0.0866025403784438,-0.4,-0.15));
#15905=CARTESIAN_POINT('',(-0.173205080756888,-0.64,-2.77555756156289E-17));
#15906=CARTESIAN_POINT('',(-0.173205080756888,-0.4,-2.12115047744981E-17));
#15907=CARTESIAN_POINT('',(-0.0866025403784438,-0.64,-0.15));
#15908=CARTESIAN_POINT('Origin',(-0.0866025403784439,-0.4,0.15));
#15909=CARTESIAN_POINT('',(-0.0866025403784439,-0.4,0.15));
#15910=CARTESIAN_POINT('',(-0.173205080756888,-0.4,-2.12115047744981E-17));
#15911=CARTESIAN_POINT('',(-0.0866025403784439,-0.64,0.15));
#15912=CARTESIAN_POINT('',(-0.0866025403784439,-0.4,0.15));
#15913=CARTESIAN_POINT('',(-0.173205080756888,-0.64,-2.12115047744981E-17));
#15914=CARTESIAN_POINT('Origin',(0.0866025403784439,-0.4,0.15));
#15915=CARTESIAN_POINT('',(0.0866025403784439,-0.4,0.15));
#15916=CARTESIAN_POINT('',(-0.0866025403784439,-0.4,0.15));
#15917=CARTESIAN_POINT('',(0.0866025403784439,-0.64,0.15));
#15918=CARTESIAN_POINT('',(0.0866025403784439,-0.4,0.15));
#15919=CARTESIAN_POINT('',(-0.0866025403784439,-0.64,0.15));
#15920=CARTESIAN_POINT('Origin',(0.173205080756888,-0.4,0.));
#15921=CARTESIAN_POINT('',(0.0866025403784439,-0.4,0.15));
#15922=CARTESIAN_POINT('',(0.0866025403784439,-0.64,0.15));
#15923=CARTESIAN_POINT('Origin',(0.,-0.4,-2.77555756156289E-17));
#15924=CARTESIAN_POINT('Origin',(0.,-0.64,-2.77555756156289E-17));
#15925=CARTESIAN_POINT('Origin',(0.,-1.,0.));
#15926=CARTESIAN_POINT('',(-0.1954,-1.,2.39295984553393E-17));
#15927=CARTESIAN_POINT('Origin',(0.,-1.,0.));
#15928=CARTESIAN_POINT('Origin',(0.3,0.4,0.));
#15929=CARTESIAN_POINT('',(-0.3,0.4,-3.67394039744206E-17));
#15930=CARTESIAN_POINT('Origin',(0.,0.4,0.));
#15931=CARTESIAN_POINT('Origin',(0.,0.375,0.));
#15932=CARTESIAN_POINT('',(-0.35,0.35,-4.28626379701573E-17));
#15933=CARTESIAN_POINT('Origin',(0.,0.35,0.));
#15934=CARTESIAN_POINT('',(-0.325,0.375,-3.9801020972289E-17));
#15935=CARTESIAN_POINT('Origin',(0.,0.19,0.));
#15936=CARTESIAN_POINT('',(-0.35,0.03,-4.28626379701574E-17));
#15937=CARTESIAN_POINT('Origin',(0.,0.03,0.));
#15938=CARTESIAN_POINT('',(-0.35,0.19,-4.28626379701574E-17));
#15939=CARTESIAN_POINT('Origin',(0.,0.0149999999999999,0.));
#15940=CARTESIAN_POINT('',(-0.32,-3.29597460435593E-17,-3.91886975727153E-17));
#15941=CARTESIAN_POINT('Origin',(0.,0.,0.));
#15942=CARTESIAN_POINT('',(-0.335,0.0149999999999999,-4.10256677714363E-17));
#15943=CARTESIAN_POINT('Origin',(0.22,0.,0.));
#15944=CARTESIAN_POINT('',(-0.22,-6.93889390390723E-18,-2.69422295812418E-17));
#15945=CARTESIAN_POINT('Origin',(0.,0.,0.));
#15946=CARTESIAN_POINT('Origin',(0.,-0.02,0.));
#15947=CARTESIAN_POINT('',(-0.1954,-0.0492,2.39295984553393E-17));
#15948=CARTESIAN_POINT('Origin',(0.,-0.0492,0.));
#15949=CARTESIAN_POINT('',(-0.21,-0.02,-2.57175827820944E-17));
#15950=CARTESIAN_POINT('Origin',(0.,-0.8,0.));
#15951=CARTESIAN_POINT('',(-0.1954,-0.8,-2.39295984553393E-17));
#17762=UNCERTAINTY_MEASURE_WITH_UNIT(LENGTH_MEASURE(0.001),#17831,
'DISTANCE_ACCURACY_VALUE',
'Maximum model space distance between geometric entities at asserted c
onnectivities');
#17780=UNCERTAINTY_MEASURE_WITH_UNIT(LENGTH_MEASURE(0.001),#17831,
'DISTANCE_ACCURACY_VALUE',
'Maximum model space distance between geometric entities at asserted c
onnectivities');
#17812=(
GEOMETRIC_REPRESENTATION_CONTEXT(3)
GLOBAL_UNCERTAINTY_ASSIGNED_CONTEXT((#17762))
GLOBAL_UNIT_ASSIGNED_CONTEXT((#17831,#17833,#17834))
REPRESENTATION_CONTEXT('','3D')
);
#17830=(
GEOMETRIC_REPRESENTATION_CONTEXT(3)
GLOBAL_UNCERTAINTY_ASSIGNED_CONTEXT((#17780))
GLOBAL_UNIT_ASSIGNED_CONTEXT((#17831,#17833,#17834))
REPRESENTATION_CONTEXT('','3D')
);
#17831=(
LENGTH_UNIT()
NAMED_UNIT(*)
SI_UNIT(.CENTI.,.METRE.)
);
#17833=(
NAMED_UNIT(*)
PLANE_ANGLE_UNIT()
SI_UNIT($,.RADIAN.)
);
#17834=(
NAMED_UNIT(*)
SI_UNIT($,.STERADIAN.)
SOLID_ANGLE_UNIT()
);
#17866=SHAPE_DEFINITION_REPRESENTATION(#17925,#18037);
#17925=PRODUCT_DEFINITION_SHAPE('',$,#18087);
#18037=SHAPE_REPRESENTATION('',(#10168),#17812);
#18055=PRODUCT_DEFINITION_CONTEXT('part definition',#18204,'design');
#18087=PRODUCT_DEFINITION('M4x10 Cap Screw','M4x10 Cap Screw',#18136,#18055);
#18136=PRODUCT_DEFINITION_FORMATION('',$,#18237);
#18204=APPLICATION_CONTEXT(
'Core Data for Automotive Mechanical Design Process');
#18205=PRODUCT_CONTEXT('part definition',#18204,'mechanical');
#18237=PRODUCT('M4x10 Cap Screw','M4x10 Cap Screw','M4x10 Cap Screw',(#18205));
#18318=COLOUR_RGB('Black',0.12,0.14,0.17);
#18319=FILL_AREA_STYLE_COLOUR('',#18318);
#18320=FILL_AREA_STYLE('',(#18319));
#18321=SURFACE_STYLE_FILL_AREA(#18320);
#18322=SURFACE_SIDE_STYLE('',(#18321));
#18323=SURFACE_STYLE_USAGE(.BOTH.,#18322);
#18324=PRESENTATION_STYLE_ASSIGNMENT((#18323));
ENDSEC;
END-ISO-10303-21;
